ISO-10303-21;
HEADER;
FILE_DESCRIPTION (('STEP AP214'),
    '1' );
FILE_NAME ('socket head cap screw_iso_ISO 4762 M5 x 20 - 20N.step',
    '2026-10-24T14:05:44',
    ( '' ),
    ( '' ),
    'SwSTEP 2.0',
    'SolidWorks 2026',
    '' );
FILE_SCHEMA (( 'AUTOMOTIVE_DESIGN' ));
ENDSEC;

DATA;
#3=ORIENTED_EDGE ( 'NONE', *, *, #1318, .T. ) ;
#11=ORIENTED_EDGE ( 'NONE', *, *, #5026, .T. ) ;
#23=VECTOR ( 'NONE', #2608, 1000.000000000000000 ) ;
#29=LINE ( 'NONE', #5746, #1486 ) ;
#30=CIRCLE ( 'NONE', #5634, 2.041999999999999815 ) ;
#32=CARTESIAN_POINT ( 'NONE',  ( 2.500000000000000000, 2.357898499370433054, -1.951563910473907981E-15 ) ) ;
#43=EDGE_CURVE ( 'NONE', #586, #2446, #6979, .T. ) ;
#48=ORIENTED_EDGE ( 'NONE', *, *, #1653, .T. ) ;
#66=CARTESIAN_POINT ( 'NONE',  ( 2.500000000000000000, 0.000000000000000000, 2.041999999999999815 ) ) ;
#69=AXIS2_PLACEMENT_3D ( 'NONE', #6445, #5876, #2455 ) ;
#70=EDGE_CURVE ( 'NONE', #2423, #6108, #5233, .T. ) ;
#81=ORIENTED_EDGE ( 'NONE', *, *, #6837, .T. ) ;
#86=DIRECTION ( 'NONE',  ( 0.000000000000000000, 0.8660254037844380415, -0.5000000000000011102 ) ) ;
#98=AXIS2_PLACEMENT_3D ( 'NONE', #2545, #1752, #6896 ) ;
#115=DIRECTION ( 'NONE',  ( 0.000000000000000000, 0.000000000000000000, -1.000000000000000000 ) ) ;
#116=CARTESIAN_POINT ( 'NONE',  ( 2.500000000000000000, 2.357898499370433054, -1.951563910473907981E-15 ) ) ;
#118=ORIENTED_EDGE ( 'NONE', *, *, #6220, .F. ) ;
#127=EDGE_LOOP ( 'NONE', ( #4208, #2738, #2635, #4055 ) ) ;
#156=CARTESIAN_POINT ( 'NONE',  ( 2.500000000000000000, -1.178949249685213863, 2.042000000000002924 ) ) ;
#160=DIRECTION ( 'NONE',  ( 0.000000000000000000, 0.000000000000000000, 1.000000000000000000 ) ) ;
#164=ORIENTED_EDGE ( 'NONE', *, *, #4721, .T. ) ;
#171=AXIS2_PLACEMENT_3D ( 'NONE', #6654, #216, #2471 ) ;
#178=DIRECTION ( 'NONE',  ( 0.000000000000000000, 0.000000000000000000, 1.000000000000000000 ) ) ;
#180=VECTOR ( 'NONE', #724, 1000.000000000000114 ) ;
#185=CIRCLE ( 'NONE', #4719, 0.2500000000000002220 ) ;
#196=FACE_OUTER_BOUND ( 'NONE', #2058, .T. ) ;
#216=DIRECTION ( 'NONE',  ( 1.000000000000000000, 0.000000000000000000, 0.000000000000000000 ) ) ;
#230=CARTESIAN_POINT ( 'NONE',  ( 24.55500000000002103, 0.000000000000000000, 0.000000000000000000 ) ) ;
#240=LINE ( 'NONE', #1936, #5296 ) ;
#248=AXIS2_PLACEMENT_3D ( 'NONE', #5345, #1301, #1857 ) ;
#251=EDGE_LOOP ( 'NONE', ( #4553, #3750, #2974 ) ) ;
#255=CARTESIAN_POINT ( 'NONE',  ( 5.000000000000002665, 3.306546357697854226E-16, 2.700000000000001066 ) ) ;
#265=( NAMED_UNIT ( * ) SI_UNIT ( $, .STERADIAN. ) SOLID_ANGLE_UNIT ( ) );
#269=CIRCLE ( 'NONE', #2514, 2.700000000000001066 ) ;
#280=ORIENTED_EDGE ( 'NONE', *, *, #5520, .F. ) ;
#288=EDGE_CURVE ( 'NONE', #5585, #1382, #4104, .T. ) ;
#290=DIRECTION ( 'NONE',  ( 0.000000000000000000, 1.000000000000000000, -1.471414886128461471E-15 ) ) ;
#313=DIRECTION ( 'NONE',  ( 0.000000000000000000, 0.000000000000000000, 1.000000000000000000 ) ) ;
#316=CARTESIAN_POINT ( 'NONE',  ( 0.2500000000000002220, 0.000000000000000000, 4.000000000000000000 ) ) ;
#318=CARTESIAN_POINT ( 'NONE',  ( 5.200000000000002842, 3.306546357697854719E-16, 2.700000000000001066 ) ) ;
#321=AXIS2_PLACEMENT_3D ( 'NONE', #471, #4507, #6798 ) ;
#326=FACE_OUTER_BOUND ( 'NONE', #3436, .T. ) ;
#350=DIRECTION ( 'NONE',  ( -1.000000000000000000, -0.000000000000000000, -0.000000000000000000 ) ) ;
#355=DIRECTION ( 'NONE',  ( 0.000000000000000000, 0.4999999999999993339, -0.8660254037844390407 ) ) ;
#364=ORIENTED_EDGE ( 'NONE', *, *, #2779, .F. ) ;
#370=ADVANCED_FACE ( 'NONE', ( #475 ), #3330, .F. ) ;
#389=DIRECTION ( 'NONE',  ( 0.000000000000000000, 1.000000000000000000, -1.471414886128461471E-15 ) ) ;
#404=ORIENTED_EDGE ( 'NONE', *, *, #43, .T. ) ;
#405=AXIS2_PLACEMENT_3D ( 'NONE', #1576, #6078, #4992 ) ;
#413=CIRCLE ( 'NONE', #4342, 0.2000000000000000944 ) ;
#418=EDGE_CURVE ( 'NONE', #7308, #2028, #4397, .T. ) ;
#429=MECHANICAL_DESIGN_GEOMETRIC_PRESENTATION_REPRESENTATION('',(#5917),#4698);
#435=CARTESIAN_POINT ( 'NONE',  ( 25.00000000000000000, 0.000000000000000000, 2.055000000000000160 ) ) ;
#463=CARTESIAN_POINT ( 'NONE',  ( 0.000000000000000000, 5.051668046482832750E-16, -4.000000000000000000 ) ) ;
#468=VERTEX_POINT ( 'NONE', #1903 ) ;
#471=CARTESIAN_POINT ( 'NONE',  ( 2.500000000000000000, 2.357898499370433054, -1.951563910473907981E-15 ) ) ;
#475=FACE_OUTER_BOUND ( 'NONE', #720, .T. ) ;
#480=DIRECTION ( 'NONE',  ( -1.000000000000000000, -0.000000000000000000, -0.000000000000000000 ) ) ;
#481=CARTESIAN_POINT ( 'NONE',  ( 0.000000000000000000, 1.178949249685213863, -2.042000000000001148 ) ) ;
#500=EDGE_CURVE ( 'NONE', #4203, #1612, #4312, .T. ) ;
#512=CARTESIAN_POINT ( 'NONE',  ( 25.00000000000000000, 0.000000000000000000, 0.000000000000000000 ) ) ;
#518=EDGE_LOOP ( 'NONE', ( #824, #118 ) ) ;
#522=SHAPE_DEFINITION_REPRESENTATION ( #2401, #951 ) ;
#534=ORIENTED_EDGE ( 'NONE', *, *, #6574, .T. ) ;
#544=CARTESIAN_POINT ( 'NONE',  ( 2.500000000000000000, -1.768423874527823791, -1.020999999999998353 ) ) ;
#560=ORIENTED_EDGE ( 'NONE', *, *, #3390, .T. ) ;
#571=DIRECTION ( 'NONE',  ( 1.000000000000000000, 0.000000000000000000, 0.000000000000000000 ) ) ;
#586=VERTEX_POINT ( 'NONE', #3703 ) ;
#589=LINE ( 'NONE', #3742, #4186 ) ;
#598=VERTEX_POINT ( 'NONE', #834 ) ;
#610=CARTESIAN_POINT ( 'NONE',  ( 0.000000000000000000, 1.178949249685218525, 2.041999999999999371 ) ) ;
#620=DIRECTION ( 'NONE',  ( -0.5000000000000051070, 0.000000000000000000, 0.8660254037844355990 ) ) ;
#626=ORIENTED_EDGE ( 'NONE', *, *, #2507, .F. ) ;
#628=DIRECTION ( 'NONE',  ( 0.000000000000000000, 0.000000000000000000, 1.000000000000000000 ) ) ;
#654=LINE ( 'NONE', #7017, #3221 ) ;
#655=CARTESIAN_POINT ( 'NONE',  ( -31.74999999999995737, 0.000000000000000000, 0.000000000000000000 ) ) ;
#656=AXIS2_PLACEMENT_3D ( 'NONE', #3631, #4731, #1283 ) ;
#691=DIRECTION ( 'NONE',  ( -0.000000000000000000, 0.8660254037844390407, 0.4999999999999993339 ) ) ;
#710=DIRECTION ( 'NONE',  ( 0.000000000000000000, 0.5000000000000011102, 0.8660254037844380415 ) ) ;
#718=UNCERTAINTY_MEASURE_WITH_UNIT (LENGTH_MEASURE( 1.000000000000000082E-05 ), #3530, 'distance_accuracy_value', 'NONE');
#720=EDGE_LOOP ( 'NONE', ( #4664, #4216, #5470 ) ) ;
#724=DIRECTION ( 'NONE',  ( 0.000000000000000000, -0.5000000000000011102, -0.8660254037844379305 ) ) ;
#739=ORIENTED_EDGE ( 'NONE', *, *, #5593, .F. ) ;
#745=FACE_OUTER_BOUND ( 'NONE', #2106, .T. ) ;
#748=LINE ( 'NONE', #4722, #3999 ) ;
#759=DIRECTION ( 'NONE',  ( 0.000000000000000000, -0.5000000000000012212, -0.8660254037844380415 ) ) ;
#762=PRODUCT_DEFINITION_FORMATION_WITH_SPECIFIED_SOURCE ( 'ANY', '', #3604, .NOT_KNOWN. ) ;
#768=EDGE_CURVE ( 'NONE', #1382, #2446, #4670, .T. ) ;
#773=ORIENTED_EDGE ( 'NONE', *, *, #4795, .T. ) ;
#801=CARTESIAN_POINT ( 'NONE',  ( 0.000000000000000000, -1.178949249685213863, 2.042000000000002924 ) ) ;
#805=ORIENTED_EDGE ( 'NONE', *, *, #5847, .F. ) ;
#815=DIRECTION ( 'NONE',  ( -1.000000000000000000, -0.000000000000000000, -0.000000000000000000 ) ) ;
#823=SURFACE_STYLE_USAGE ( .BOTH. , #1821 ) ;
#824=ORIENTED_EDGE ( 'NONE', *, *, #1455, .F. ) ;
#834=CARTESIAN_POINT ( 'NONE',  ( 25.00000000000000000, 0.000000000000000000, 2.055000000000000160 ) ) ;
#850=DIRECTION ( 'NONE',  ( 1.000000000000000000, 0.000000000000000000, 0.000000000000000000 ) ) ;
#854=PLANE ( 'NONE',  #405 ) ;
#857=VECTOR ( 'NONE', #3808, 1000.000000000000000 ) ;
#878=ADVANCED_FACE ( 'NONE', ( #5487 ), #4258, .F. ) ;
#879=CARTESIAN_POINT ( 'NONE',  ( 2.500000000000000000, 2.357898499370433054, -1.951563910473907981E-15 ) ) ;
#880=AXIS2_PLACEMENT_3D ( 'NONE', #156, #86, #710 ) ;
#908=DIRECTION ( 'NONE',  ( -0.7071067811865306973, 0.000000000000000000, 0.7071067811865643371 ) ) ;
#933=CARTESIAN_POINT ( 'NONE',  ( 2.500000000000000000, -1.178949249685218303, -2.041999999999998039 ) ) ;
#938=ORIENTED_EDGE ( 'NONE', *, *, #6072, .T. ) ;
#951=SHAPE_REPRESENTATION ( 'socket head cap screw_iso_ISO 4762 M5 x 20 - 20N', ( #1963 ), #4003 ) ;
#973=PLANE ( 'NONE',  #6249 ) ;
#977=VERTEX_POINT ( 'NONE', #1566 ) ;
#982=FACE_OUTER_BOUND ( 'NONE', #1058, .T. ) ;
#987=VECTOR ( 'NONE', #815, 1000.000000000000000 ) ;
#991=EDGE_LOOP ( 'NONE', ( #5668, #2360, #2719, #1798 ) ) ;
#1007=VECTOR ( 'NONE', #5328, 1000.000000000000000 ) ;
#1012=VECTOR ( 'NONE', #620, 1000.000000000000114 ) ;
#1031=CARTESIAN_POINT ( 'NONE',  ( 2.500000000000000000, 1.178949249685213863, -2.042000000000001148 ) ) ;
#1038=FACE_BOUND ( 'NONE', #5519, .T. ) ;
#1048=LINE ( 'NONE', #7298, #4130 ) ;
#1053=MECHANICAL_DESIGN_GEOMETRIC_PRESENTATION_REPRESENTATION('',(#6545),#1983);
#1058=EDGE_LOOP ( 'NONE', ( #4774, #6983, #2551, #626 ) ) ;
#1066=CARTESIAN_POINT ( 'NONE',  ( 5.000000000000002665, 0.000000000000000000, -2.700000000000001066 ) ) ;
#1090=ORIENTED_EDGE ( 'NONE', *, *, #288, .F. ) ;
#1093=ORIENTED_EDGE ( 'NONE', *, *, #5913, .F. ) ;
#1099=VECTOR ( 'NONE', #2386, 1000.000000000000000 ) ;
#1102=ORIENTED_EDGE ( 'NONE', *, *, #4356, .T. ) ;
#1104=CARTESIAN_POINT ( 'NONE',  ( 2.500000000000000000, 0.000000000000000000, 0.000000000000000000 ) ) ;
#1105=CARTESIAN_POINT ( 'NONE',  ( 2.500000000000000000, 2.500728763858895382E-16, -2.041999999999999815 ) ) ;
#1125=AXIS2_PLACEMENT_3D ( 'NONE', #1511, #4353, #5626 ) ;
#1146=CARTESIAN_POINT ( 'NONE',  ( 2.500000000000000000, 2.357898499370433054, -1.951563910473907981E-15 ) ) ;
#1180=DIRECTION ( 'NONE',  ( 0.000000000000000000, 0.000000000000000000, 1.000000000000000000 ) ) ;
#1182=LINE ( 'NONE', #1105, #6356 ) ;
#1183=CARTESIAN_POINT ( 'NONE',  ( 2.500000000000000000, -2.357898499370432610, 3.252606517456513302E-15 ) ) ;
#1185=ORIENTED_EDGE ( 'NONE', *, *, #3609, .F. ) ;
#1194=ORIENTED_EDGE ( 'NONE', *, *, #3551, .T. ) ;
#1200=APPLICATION_CONTEXT ( 'automotive_design' ) ;
#1210=LINE ( 'NONE', #3476, #1099 ) ;
#1235=FACE_OUTER_BOUND ( 'NONE', #5839, .T. ) ;
#1276=ORIENTED_EDGE ( 'NONE', *, *, #2307, .T. ) ;
#1280=DIRECTION ( 'NONE',  ( 0.000000000000000000, 0.000000000000000000, 1.000000000000000000 ) ) ;
#1283=DIRECTION ( 'NONE',  ( 0.000000000000000000, 0.000000000000000000, -1.000000000000000000 ) ) ;
#1301=DIRECTION ( 'NONE',  ( 1.000000000000000000, 0.000000000000000000, 0.000000000000000000 ) ) ;
#1309=DIRECTION ( 'NONE',  ( 0.000000000000000000, -0.4999999999999993894, 0.8660254037844389297 ) ) ;
#1313=CIRCLE ( 'NONE', #5497, 2.500000000000001332 ) ;
#1318=EDGE_CURVE ( 'NONE', #2488, #2773, #2508, .T. ) ;
#1320=ORIENTED_EDGE ( 'NONE', *, *, #4174, .T. ) ;
#1350=VECTOR ( 'NONE', #759, 999.9999999999998863 ) ;
#1355=CARTESIAN_POINT ( 'NONE',  ( 0.000000000000000000, 1.178949249685213863, -2.042000000000001148 ) ) ;
#1363=VECTOR ( 'NONE', #389, 1000.000000000000000 ) ;
#1382=VERTEX_POINT ( 'NONE', #3213 ) ;
#1384=ORIENTED_EDGE ( 'NONE', *, *, #5683, .T. ) ;
#1389=CARTESIAN_POINT ( 'NONE',  ( 2.500000000000000000, 0.000000000000000000, 0.000000000000000000 ) ) ;
#1399=CARTESIAN_POINT ( 'NONE',  ( -31.74999999999995737, 0.000000000000000000, 0.000000000000000000 ) ) ;
#1406=EDGE_CURVE ( 'NONE', #6247, #5197, #3713, .T. ) ;
#1412=DIRECTION ( 'NONE',  ( 0.000000000000000000, -1.287488025362403787E-15, -1.000000000000000000 ) ) ;
#1416=FACE_OUTER_BOUND ( 'NONE', #251, .T. ) ;
#1419=VERTEX_POINT ( 'NONE', #6696 ) ;
#1428=DIRECTION ( 'NONE',  ( 0.000000000000000000, 0.000000000000000000, 1.000000000000000000 ) ) ;
#1430=APPLICATION_CONTEXT ( 'automotive_design' ) ;
#1433=LINE ( 'NONE', #6058, #3614 ) ;
#1435=EDGE_CURVE ( 'NONE', #4318, #3965, #2809, .T. ) ;
#1447=LINE ( 'NONE', #5489, #857 ) ;
#1451=ORIENTED_EDGE ( 'NONE', *, *, #5683, .F. ) ;
#1455=EDGE_CURVE ( 'NONE', #598, #3083, #6300, .T. ) ;
#1464=CARTESIAN_POINT ( 'NONE',  ( 0.2500000000000002220, 0.000000000000000000, 0.000000000000000000 ) ) ;
#1486=VECTOR ( 'NONE', #2324, 999.9999999999998863 ) ;
#1511=CARTESIAN_POINT ( 'NONE',  ( 2.500000000000000000, 2.357898499370433054, -1.951563910473907981E-15 ) ) ;
#1521=CARTESIAN_POINT ( 'NONE',  ( 25.00000000000000000, 2.789133085058098087E-16, -2.055000000000000160 ) ) ;
#1549=ADVANCED_FACE ( 'NONE', ( #1038, #3828 ), #6127, .T. ) ;
#1555=( LENGTH_UNIT ( ) NAMED_UNIT ( * ) SI_UNIT ( .MILLI., .METRE. ) );
#1556=DIRECTION ( 'NONE',  ( 0.000000000000000000, 0.000000000000000000, 1.000000000000000000 ) ) ;
#1559=EDGE_LOOP ( 'NONE', ( #4249, #164, #4770 ) ) ;
#1566=CARTESIAN_POINT ( 'NONE',  ( 2.500000000000000000, 1.768423874527824902, 1.020999999999999019 ) ) ;
#1571=EDGE_CURVE ( 'NONE', #3704, #2028, #6180, .T. ) ;
#1576=CARTESIAN_POINT ( 'NONE',  ( 0.000000000000000000, 0.000000000000000000, 0.000000000000000000 ) ) ;
#1581=CARTESIAN_POINT ( 'NONE',  ( 2.500000000000000000, -1.178949249685213863, 2.042000000000002924 ) ) ;
#1592=DIRECTION ( 'NONE',  ( 0.000000000000000000, 0.000000000000000000, -1.000000000000000000 ) ) ;
#1608=DIRECTION ( 'NONE',  ( -1.000000000000000000, -0.000000000000000000, -0.000000000000000000 ) ) ;
#1612=VERTEX_POINT ( 'NONE', #6278 ) ;
#1615=ORIENTED_EDGE ( 'NONE', *, *, #5724, .T. ) ;
#1617=PLANE ( 'NONE',  #321 ) ;
#1620=DIRECTION ( 'NONE',  ( 0.000000000000000000, -1.224646799147353454E-16, 1.000000000000000000 ) ) ;
#1632=FACE_OUTER_BOUND ( 'NONE', #1559, .T. ) ;
#1634=ORIENTED_EDGE ( 'NONE', *, *, #6220, .T. ) ;
#1653=EDGE_CURVE ( 'NONE', #977, #2773, #5851, .T. ) ;
#1657=DIRECTION ( 'NONE',  ( 0.000000000000000000, -1.000000000000000000, 0.000000000000000000 ) ) ;
#1665=DIRECTION ( 'NONE',  ( -0.5000000000000051070, 1.060575238724903217E-16, -0.8660254037844355990 ) ) ;
#1677=ADVANCED_FACE ( 'NONE', ( #2284 ), #4685, .T. ) ;
#1685=ORIENTED_EDGE ( 'NONE', *, *, #5635, .F. ) ;
#1688=CARTESIAN_POINT ( 'NONE',  ( 2.500000000000000000, 1.178949249685218525, 2.041999999999999371 ) ) ;
#1699=ADVANCED_FACE ( 'NONE', ( #5779 ), #4127, .T. ) ;
#1718=ORIENTED_EDGE ( 'NONE', *, *, #4396, .T. ) ;
#1726=DIRECTION ( 'NONE',  ( -0.000000000000000000, 1.000000000000000000, 1.224646799147353207E-16 ) ) ;
#1744=PRODUCT_CONTEXT ( 'NONE', #1430, 'mechanical' ) ;
#1752=DIRECTION ( 'NONE',  ( 1.000000000000000000, 0.000000000000000000, 0.000000000000000000 ) ) ;
#1757=PLANE ( 'NONE',  #880 ) ;
#1797=LINE ( 'NONE', #5891, #1350 ) ;
#1798=ORIENTED_EDGE ( 'NONE', *, *, #2307, .F. ) ;
#1810=CARTESIAN_POINT ( 'NONE',  ( 3.678949249685231848, 0.000000000000000000, 0.000000000000000000 ) ) ;
#1821=SURFACE_SIDE_STYLE ('',( #5958 ) ) ;
#1826=AXIS2_PLACEMENT_3D ( 'NONE', #3823, #2768, #4429 ) ;
#1850=VECTOR ( 'NONE', #5715, 1000.000000000000114 ) ;
#1857=DIRECTION ( 'NONE',  ( 0.000000000000000000, 0.000000000000000000, -1.000000000000000000 ) ) ;
#1866=ORIENTED_EDGE ( 'NONE', *, *, #3370, .F. ) ;
#1875=EDGE_CURVE ( 'NONE', #6108, #4203, #1048, .T. ) ;
#1903=CARTESIAN_POINT ( 'NONE',  ( 24.55500000000002103, 0.000000000000000000, 2.500000000000001332 ) ) ;
#1908=ADVANCED_FACE ( 'NONE', ( #5588 ), #1617, .F. ) ;
#1913=CARTESIAN_POINT ( 'NONE',  ( 2.500000000000000000, 0.000000000000000000, 0.000000000000000000 ) ) ;
#1928=DIRECTION ( 'NONE',  ( -1.000000000000000000, -0.000000000000000000, -0.000000000000000000 ) ) ;
#1930=AXIS2_PLACEMENT_3D ( 'NONE', #5601, #3258, #1556 ) ;
#1931=CLOSED_SHELL ( 'NONE', ( #4973, #2450, #5528, #2325, #5277, #4629, #2928, #3996, #6463, #6591, #1549, #1699, #2441, #5052, #3178, #6010, #5335, #1677, #878, #4901, #4099, #370, #3043, #7043, #1908, #3932, #5821 ) ) ;
#1936=CARTESIAN_POINT ( 'NONE',  ( 2.500000000000000000, 2.357898499370433054, -1.951563910473907981E-15 ) ) ;
#1956=ORIENTED_EDGE ( 'NONE', *, *, #6241, .T. ) ;
#1963=AXIS2_PLACEMENT_3D ( 'NONE', #2294, #628, #5829 ) ;
#1973=FACE_BOUND ( 'NONE', #5709, .T. ) ;
#1981=CARTESIAN_POINT ( 'NONE',  ( 2.500000000000000000, -2.357898499370432610, 3.252606517456513302E-15 ) ) ;
#1983=( GEOMETRIC_REPRESENTATION_CONTEXT ( 3 ) GLOBAL_UNCERTAINTY_ASSIGNED_CONTEXT ( ( #718 ) ) GLOBAL_UNIT_ASSIGNED_CONTEXT ( ( #3530, #5599, #5042 ) ) REPRESENTATION_CONTEXT ( 'NONE', 'WORKASPACE' ) );
#2009=FACE_OUTER_BOUND ( 'NONE', #4385, .T. ) ;
#2013=CARTESIAN_POINT ( 'NONE',  ( 0.000000000000000000, -2.357898499370432610, 3.252606517456513302E-15 ) ) ;
#2017=DIRECTION ( 'NONE',  ( -1.000000000000000000, -0.000000000000000000, -0.000000000000000000 ) ) ;
#2019=DIRECTION ( 'NONE',  ( -1.000000000000000000, -0.000000000000000000, -0.000000000000000000 ) ) ;
#2028=VERTEX_POINT ( 'NONE', #2310 ) ;
#2030=CIRCLE ( 'NONE', #6477, 2.041999999999999815 ) ;
#2058=EDGE_LOOP ( 'NONE', ( #5443, #81, #6928 ) ) ;
#2065=TOROIDAL_SURFACE ( 'NONE', #171, 2.700000000000001066, 0.2000000000000000111 ) ;
#2072=VERTEX_POINT ( 'NONE', #610 ) ;
#2103=DIRECTION ( 'NONE',  ( -1.000000000000000000, -0.000000000000000000, -0.000000000000000000 ) ) ;
#2106=EDGE_LOOP ( 'NONE', ( #6829, #534, #1276, #4886 ) ) ;
#2133=CARTESIAN_POINT ( 'NONE',  ( 2.500000000000000000, 0.000000000000000000, 0.000000000000000000 ) ) ;
#2142=DIRECTION ( 'NONE',  ( 0.000000000000000000, 0.000000000000000000, -1.000000000000000000 ) ) ;
#2171=UNCERTAINTY_MEASURE_WITH_UNIT (LENGTH_MEASURE( 1.000000000000000082E-05 ), #3079, 'distance_accuracy_value', 'NONE');
#2173=AXIS2_PLACEMENT_3D ( 'NONE', #6144, #1608, #3891 ) ;
#2190=EDGE_CURVE ( 'NONE', #2488, #977, #5788, .T. ) ;
#2219=DIRECTION ( 'NONE',  ( 0.000000000000000000, -0.5000000000000011102, -0.8660254037844379305 ) ) ;
#2264=CARTESIAN_POINT ( 'NONE',  ( 5.000000000000000888, 0.000000000000000000, 0.000000000000000000 ) ) ;
#2276=CARTESIAN_POINT ( 'NONE',  ( 5.200000000000002842, 0.000000000000000000, -2.700000000000001066 ) ) ;
#2284=FACE_OUTER_BOUND ( 'NONE', #2392, .T. ) ;
#2294=CARTESIAN_POINT ( 'NONE',  ( 0.000000000000000000, 0.000000000000000000, 0.000000000000000000 ) ) ;
#2301=AXIS2_PLACEMENT_3D ( 'NONE', #3746, #7283, #5431 ) ;
#2303=ORIENTED_EDGE ( 'NONE', *, *, #5865, .T. ) ;
#2305=CIRCLE ( 'NONE', #656, 2.500000000000000888 ) ;
#2307=EDGE_CURVE ( 'NONE', #468, #1419, #1433, .T. ) ;
#2310=CARTESIAN_POINT ( 'NONE',  ( 2.500000000000000000, -1.768423874527823569, 1.021000000000002794 ) ) ;
#2314=CIRCLE ( 'NONE', #2539, 2.055000000000000160 ) ;
#2315=( NAMED_UNIT ( * ) SI_UNIT ( $, .STERADIAN. ) SOLID_ANGLE_UNIT ( ) );
#2324=DIRECTION ( 'NONE',  ( 0.000000000000000000, -0.5000000000000012212, -0.8660254037844380415 ) ) ;
#2325=ADVANCED_FACE ( 'NONE', ( #3027 ), #7057, .T. ) ;
#2329=ORIENTED_EDGE ( 'NONE', *, *, #2527, .T. ) ;
#2360=ORIENTED_EDGE ( 'NONE', *, *, #1406, .T. ) ;
#2366=ORIENTED_EDGE ( 'NONE', *, *, #5593, .T. ) ;
#2373=AXIS2_PLACEMENT_3D ( 'NONE', #2133, #6118, #6000 ) ;
#2386=DIRECTION ( 'NONE',  ( 0.000000000000000000, 1.000000000000000000, -1.471414886128461471E-15 ) ) ;
#2387=CIRCLE ( 'NONE', #3464, 2.700000000000001066 ) ;
#2389=DIRECTION ( 'NONE',  ( -0.000000000000000000, 1.471414886128461471E-15, 1.000000000000000000 ) ) ;
#2392=EDGE_LOOP ( 'NONE', ( #3219, #805, #6638, #11, #6012 ) ) ;
#2401=PRODUCT_DEFINITION_SHAPE ( 'NONE', 'NONE',  #3304 ) ;
#2410=VECTOR ( 'NONE', #355, 1000.000000000000000 ) ;
#2411=VECTOR ( 'NONE', #3532, 999.9999999999998863 ) ;
#2423=VERTEX_POINT ( 'NONE', #2618 ) ;
#2441=ADVANCED_FACE ( 'NONE', ( #4918 ), #2065, .F. ) ;
#2446=VERTEX_POINT ( 'NONE', #4769 ) ;
#2450=ADVANCED_FACE ( 'NONE', ( #4361 ), #4818, .T. ) ;
#2455=DIRECTION ( 'NONE',  ( 0.000000000000000000, 0.000000000000000000, 1.000000000000000000 ) ) ;
#2456=SHAPE_REPRESENTATION_RELATIONSHIP ( 'NONE' , 'NONE' ,  #951, #7090 ) ;
#2459=EDGE_CURVE ( 'NONE', #6041, #3704, #4958, .T. ) ;
#2468=VERTEX_POINT ( 'NONE', #2013 ) ;
#2471=DIRECTION ( 'NONE',  ( 0.000000000000000000, 0.000000000000000000, -1.000000000000000000 ) ) ;
#2484=DIRECTION ( 'NONE',  ( 0.000000000000000000, 0.000000000000000000, -1.000000000000000000 ) ) ;
#2488=VERTEX_POINT ( 'NONE', #6687 ) ;
#2497=EDGE_CURVE ( 'NONE', #5368, #1612, #5002, .T. ) ;
#2500=ORIENTED_EDGE ( 'NONE', *, *, #3370, .T. ) ;
#2507=EDGE_CURVE ( 'NONE', #3965, #4318, #4592, .T. ) ;
#2508=LINE ( 'NONE', #6097, #5711 ) ;
#2512=LINE ( 'NONE', #2678, #5198 ) ;
#2514=AXIS2_PLACEMENT_3D ( 'NONE', #2264, #4532, #6822 ) ;
#2527=EDGE_CURVE ( 'NONE', #1419, #7102, #413, .T. ) ;
#2530=DIRECTION ( 'NONE',  ( 0.000000000000000000, 0.5000000000000012212, 0.8660254037844380415 ) ) ;
#2536=AXIS2_PLACEMENT_3D ( 'NONE', #4738, #2794, #178 ) ;
#2539=AXIS2_PLACEMENT_3D ( 'NONE', #6598, #5504, #4428 ) ;
#2545=CARTESIAN_POINT ( 'NONE',  ( 0.2500000000000002220, 0.000000000000000000, 0.000000000000000000 ) ) ;
#2551=ORIENTED_EDGE ( 'NONE', *, *, #3609, .T. ) ;
#2558=AXIS2_PLACEMENT_3D ( 'NONE', #5671, #7287, #2142 ) ;
#2569=ORIENTED_EDGE ( 'NONE', *, *, #1875, .T. ) ;
#2606=ORIENTED_EDGE ( 'NONE', *, *, #3748, .F. ) ;
#2608=DIRECTION ( 'NONE',  ( 0.000000000000000000, 0.4999999999999993339, -0.8660254037844390407 ) ) ;
#2618=CARTESIAN_POINT ( 'NONE',  ( 2.500000000000000000, 1.768423874527822681, -1.021000000000002794 ) ) ;
#2635=ORIENTED_EDGE ( 'NONE', *, *, #3800, .T. ) ;
#2639=PLANE ( 'NONE',  #3719 ) ;
#2644=VECTOR ( 'NONE', #908, 1000.000000000000000 ) ;
#2665=DIRECTION ( 'NONE',  ( 0.000000000000000000, 0.000000000000000000, 1.000000000000000000 ) ) ;
#2678=CARTESIAN_POINT ( 'NONE',  ( 25.00000000000000000, 2.516649172247811061E-16, -2.055000000000000160 ) ) ;
#2697=LINE ( 'NONE', #1581, #4929 ) ;
#2699=CARTESIAN_POINT ( 'NONE',  ( 2.500000000000000000, -1.178949249685213863, 2.042000000000002924 ) ) ;
#2719=ORIENTED_EDGE ( 'NONE', *, *, #5305, .T. ) ;
#2720=CARTESIAN_POINT ( 'NONE',  ( 5.000000000000004441, 0.000000000000000000, 4.250000000000000000 ) ) ;
#2733=DIRECTION ( 'NONE',  ( -1.000000000000000000, -0.000000000000000000, -0.000000000000000000 ) ) ;
#2738=ORIENTED_EDGE ( 'NONE', *, *, #5305, .F. ) ;
#2751=DIRECTION ( 'NONE',  ( -1.000000000000000000, -0.000000000000000000, -0.000000000000000000 ) ) ;
#2763=EDGE_LOOP ( 'NONE', ( #3110, #4745 ) ) ;
#2764=DIRECTION ( 'NONE',  ( -1.000000000000000000, -0.000000000000000000, -0.000000000000000000 ) ) ;
#2768=DIRECTION ( 'NONE',  ( -1.000000000000000000, -0.000000000000000000, -0.000000000000000000 ) ) ;
#2773=VERTEX_POINT ( 'NONE', #6969 ) ;
#2779=EDGE_CURVE ( 'NONE', #3365, #2803, #748, .T. ) ;
#2782=ORIENTED_EDGE ( 'NONE', *, *, #4396, .F. ) ;
#2794=DIRECTION ( 'NONE',  ( -1.000000000000000000, -0.000000000000000000, -0.000000000000000000 ) ) ;
#2803=VERTEX_POINT ( 'NONE', #5815 ) ;
#2809=CIRCLE ( 'NONE', #5811, 4.000000000000000000 ) ;
#2814=DIRECTION ( 'NONE',  ( 0.000000000000000000, 0.000000000000000000, 1.000000000000000000 ) ) ;
#2817=DIRECTION ( 'NONE',  ( -1.000000000000000000, -0.000000000000000000, -0.000000000000000000 ) ) ;
#2839=CARTESIAN_POINT ( 'NONE',  ( 0.2500000000000002220, 4.898587196589412829E-16, -4.000000000000000000 ) ) ;
#2870=( NAMED_UNIT ( * ) PLANE_ANGLE_UNIT ( ) SI_UNIT ( $, .RADIAN. ) );
#2913=DIRECTION ( 'NONE',  ( 0.000000000000000000, 0.000000000000000000, 1.000000000000000000 ) ) ;
#2917=VECTOR ( 'NONE', #3066, 1000.000000000000000 ) ;
#2919=EDGE_LOOP ( 'NONE', ( #6079, #6549, #6953, #3320, #2569 ) ) ;
#2928=ADVANCED_FACE ( 'NONE', ( #1973, #7190 ), #854, .T. ) ;
#2938=ORIENTED_EDGE ( 'NONE', *, *, #5000, .F. ) ;
#2944=DIRECTION ( 'NONE',  ( 0.000000000000000000, -0.4999999999999993894, 0.8660254037844389297 ) ) ;
#2967=PLANE ( 'NONE',  #3594 ) ;
#2974=ORIENTED_EDGE ( 'NONE', *, *, #3018, .F. ) ;
#2976=CARTESIAN_POINT ( 'NONE',  ( 2.500000000000000000, -2.357898499370432610, 3.252606517456513302E-15 ) ) ;
#2981=CARTESIAN_POINT ( 'NONE',  ( 2.500000000000000000, 2.357898499370433054, -1.951563910473907981E-15 ) ) ;
#2996=DIRECTION ( 'NONE',  ( 1.000000000000000000, 0.000000000000000000, 0.000000000000000000 ) ) ;
#3018=EDGE_CURVE ( 'NONE', #5618, #3704, #6017, .T. ) ;
#3021=CONICAL_SURFACE ( 'NONE', #69, 2.055000000000000160, 0.7853981633974721488 ) ;
#3027=FACE_OUTER_BOUND ( 'NONE', #3073, .T. ) ;
#3043=ADVANCED_FACE ( 'NONE', ( #1632 ), #4321, .F. ) ;
#3066=DIRECTION ( 'NONE',  ( -1.000000000000000000, -0.000000000000000000, -0.000000000000000000 ) ) ;
#3070=DIRECTION ( 'NONE',  ( -1.000000000000000000, -0.000000000000000000, -0.000000000000000000 ) ) ;
#3073=EDGE_LOOP ( 'NONE', ( #6676, #6251, #1384, #5488 ) ) ;
#3075=EDGE_LOOP ( 'NONE', ( #4482, #2329, #739, #7082 ) ) ;
#3079=( LENGTH_UNIT ( ) NAMED_UNIT ( * ) SI_UNIT ( .MILLI., .METRE. ) );
#3083=VERTEX_POINT ( 'NONE', #1521 ) ;
#3110=ORIENTED_EDGE ( 'NONE', *, *, #1435, .T. ) ;
#3120=EDGE_CURVE ( 'NONE', #5618, #5368, #3833, .T. ) ;
#3130=AXIS2_PLACEMENT_3D ( 'NONE', #6976, #2389, #5853 ) ;
#3147=DIRECTION ( 'NONE',  ( -0.7071067811865306973, 8.659560562355138702E-17, -0.7071067811865643371 ) ) ;
#3162=LINE ( 'NONE', #5462, #23 ) ;
#3178=ADVANCED_FACE ( 'NONE', ( #4053 ), #3918, .T. ) ;
#3185=DIRECTION ( 'NONE',  ( 0.000000000000000000, 1.000000000000000000, -1.287488025362403787E-15 ) ) ;
#3196=ORIENTED_EDGE ( 'NONE', *, *, #1455, .T. ) ;
#3211=AXIS2_PLACEMENT_3D ( 'NONE', #5139, #2764, #3975 ) ;
#3213=CARTESIAN_POINT ( 'NONE',  ( 5.000000000000004441, 5.204748896376250699E-16, -4.250000000000000000 ) ) ;
#3219=ORIENTED_EDGE ( 'NONE', *, *, #5476, .F. ) ;
#3221=VECTOR ( 'NONE', #1309, 1000.000000000000114 ) ;
#3227=CIRCLE ( 'NONE', #6604, 0.2000000000000000944 ) ;
#3230=CARTESIAN_POINT ( 'NONE',  ( 25.00000000000000000, 2.055000000000000160, 0.000000000000000000 ) ) ;
#3239=PLANE ( 'NONE',  #3706 ) ;
#3255=CARTESIAN_POINT ( 'NONE',  ( 5.000000000000000888, 0.000000000000000000, 0.000000000000000000 ) ) ;
#3257=FILL_AREA_STYLE_COLOUR ( '', #4962 ) ;
#3258=DIRECTION ( 'NONE',  ( -1.000000000000000000, -0.000000000000000000, -0.000000000000000000 ) ) ;
#3292=UNCERTAINTY_MEASURE_WITH_UNIT (LENGTH_MEASURE( 1.000000000000000082E-05 ), #1555, 'distance_accuracy_value', 'NONE');
#3304=PRODUCT_DEFINITION ( 'UNKNOWN', '', #762, #3909 ) ;
#3320=ORIENTED_EDGE ( 'NONE', *, *, #6837, .F. ) ;
#3330=PLANE ( 'NONE',  #1125 ) ;
#3365=VERTEX_POINT ( 'NONE', #2981 ) ;
#3370=EDGE_CURVE ( 'NONE', #3365, #2423, #1797, .T. ) ;
#3384=ORIENTED_EDGE ( 'NONE', *, *, #4721, .F. ) ;
#3387=VECTOR ( 'NONE', #5001, 1000.000000000000114 ) ;
#3390=EDGE_CURVE ( 'NONE', #3365, #977, #240, .T. ) ;
#3424=ORIENTED_EDGE ( 'NONE', *, *, #6574, .F. ) ;
#3435=ORIENTED_EDGE ( 'NONE', *, *, #5476, .T. ) ;
#3436=EDGE_LOOP ( 'NONE', ( #2782, #2303, #7011, #6195, #1320 ) ) ;
#3447=CARTESIAN_POINT ( 'NONE',  ( 0.000000000000000000, 0.000000000000000000, 4.000000000000000000 ) ) ;
#3456=CIRCLE ( 'NONE', #248, 2.500000000000000888 ) ;
#3464=AXIS2_PLACEMENT_3D ( 'NONE', #3255, #4437, #1592 ) ;
#3476=CARTESIAN_POINT ( 'NONE',  ( 2.500000000000000000, -1.178949249685213863, 2.042000000000002924 ) ) ;
#3514=VECTOR ( 'NONE', #4604, 1000.000000000000000 ) ;
#3530=( LENGTH_UNIT ( ) NAMED_UNIT ( * ) SI_UNIT ( .MILLI., .METRE. ) );
#3532=DIRECTION ( 'NONE',  ( 0.000000000000000000, -0.5000000000000012212, -0.8660254037844380415 ) ) ;
#3535=VERTEX_POINT ( 'NONE', #801 ) ;
#3537=CARTESIAN_POINT ( 'NONE',  ( -31.74999999999995737, 0.000000000000000000, 0.000000000000000000 ) ) ;
#3545=ORIENTED_EDGE ( 'NONE', *, *, #5847, .T. ) ;
#3551=EDGE_CURVE ( 'NONE', #598, #468, #5032, .T. ) ;
#3570=TOROIDAL_SURFACE ( 'NONE', #3211, 4.000000000000000000, 0.2500000000000000000 ) ;
#3578=EDGE_CURVE ( 'NONE', #7308, #3535, #2697, .T. ) ;
#3579=AXIS2_PLACEMENT_3D ( 'NONE', #512, #5178, #1180 ) ;
#3580=AXIS2_PLACEMENT_3D ( 'NONE', #4403, #2019, #2665 ) ;
#3581=ORIENTED_EDGE ( 'NONE', *, *, #768, .F. ) ;
#3594=AXIS2_PLACEMENT_3D ( 'NONE', #5275, #4752, #2484 ) ;
#3604=PRODUCT ( 'socket head cap screw_iso_ISO 4762 M5 x 20 - 20N', 'socket head cap screw_iso_ISO 4762 M5 x 20 - 20N', '', ( #1744 ) ) ;
#3609=EDGE_CURVE ( 'NONE', #586, #4318, #6491, .T. ) ;
#3614=VECTOR ( 'NONE', #2017, 1000.000000000000000 ) ;
#3631=CARTESIAN_POINT ( 'NONE',  ( 5.200000000000002842, 0.000000000000000000, 0.000000000000000000 ) ) ;
#3651=ORIENTED_EDGE ( 'NONE', *, *, #6241, .F. ) ;
#3653=DIRECTION ( 'NONE',  ( -1.000000000000000000, -0.000000000000000000, -0.000000000000000000 ) ) ;
#3666=PLANE ( 'NONE',  #3130 ) ;
#3687=LINE ( 'NONE', #6630, #6255 ) ;
#3703=CARTESIAN_POINT ( 'NONE',  ( 0.2500000000000002220, 0.000000000000000000, 4.250000000000000000 ) ) ;
#3704=VERTEX_POINT ( 'NONE', #544 ) ;
#3706=AXIS2_PLACEMENT_3D ( 'NONE', #4867, #4347, #2530 ) ;
#3713=LINE ( 'NONE', #6016, #2917 ) ;
#3719=AXIS2_PLACEMENT_3D ( 'NONE', #4938, #850, #5416 ) ;
#3733=AXIS2_PLACEMENT_3D ( 'NONE', #4813, #2996, #7109 ) ;
#3736=ORIENTED_EDGE ( 'NONE', *, *, #1571, .T. ) ;
#3742=CARTESIAN_POINT ( 'NONE',  ( 2.500000000000000000, -1.178949249685213863, 2.042000000000002924 ) ) ;
#3746=CARTESIAN_POINT ( 'NONE',  ( 0.000000000000000000, 0.000000000000000000, 0.000000000000000000 ) ) ;
#3748=EDGE_CURVE ( 'NONE', #2773, #2072, #5142, .T. ) ;
#3750=ORIENTED_EDGE ( 'NONE', *, *, #5026, .F. ) ;
#3758=AXIS2_PLACEMENT_3D ( 'NONE', #4753, #5312, #7076 ) ;
#3782=FACE_OUTER_BOUND ( 'NONE', #5638, .T. ) ;
#3800=EDGE_CURVE ( 'NONE', #5197, #6342, #3227, .T. ) ;
#3808=DIRECTION ( 'NONE',  ( -1.000000000000000000, -0.000000000000000000, -0.000000000000000000 ) ) ;
#3818=CARTESIAN_POINT ( 'NONE',  ( 24.55500000000002103, 0.000000000000000000, 0.000000000000000000 ) ) ;
#3823=CARTESIAN_POINT ( 'NONE',  ( 5.000000000000004441, 0.000000000000000000, 0.000000000000000000 ) ) ;
#3828=FACE_OUTER_BOUND ( 'NONE', #5974, .T. ) ;
#3833=LINE ( 'NONE', #7169, #6497 ) ;
#3837=EDGE_LOOP ( 'NONE', ( #3196, #5860, #2938, #4723 ) ) ;
#3883=ORIENTED_EDGE ( 'NONE', *, *, #2190, .F. ) ;
#3891=DIRECTION ( 'NONE',  ( 0.000000000000000000, 0.000000000000000000, 1.000000000000000000 ) ) ;
#3909=PRODUCT_DEFINITION_CONTEXT ( 'detailed design', #1200, 'design' ) ;
#3913=FACE_OUTER_BOUND ( 'NONE', #3837, .T. ) ;
#3914=DIRECTION ( 'NONE',  ( 0.000000000000000000, 0.000000000000000000, 1.000000000000000000 ) ) ;
#3918=PLANE ( 'NONE',  #6982 ) ;
#3932=ADVANCED_FACE ( 'NONE', ( #196 ), #2967, .F. ) ;
#3942=DIRECTION ( 'NONE',  ( 0.000000000000000000, 0.000000000000000000, -1.000000000000000000 ) ) ;
#3950=CARTESIAN_POINT ( 'NONE',  ( 25.00000000000000000, 0.000000000000000000, 0.000000000000000000 ) ) ;
#3965=VERTEX_POINT ( 'NONE', #463 ) ;
#3975=DIRECTION ( 'NONE',  ( 0.000000000000000000, 0.000000000000000000, 1.000000000000000000 ) ) ;
#3988=AXIS2_PLACEMENT_3D ( 'NONE', #879, #4968, #7255 ) ;
#3996=ADVANCED_FACE ( 'NONE', ( #5490 ), #973, .T. ) ;
#3999=VECTOR ( 'NONE', #1928, 1000.000000000000000 ) ;
#4003=( GEOMETRIC_REPRESENTATION_CONTEXT ( 3 ) GLOBAL_UNCERTAINTY_ASSIGNED_CONTEXT ( ( #3292 ) ) GLOBAL_UNIT_ASSIGNED_CONTEXT ( ( #1555, #2870, #2315 ) ) REPRESENTATION_CONTEXT ( 'NONE', 'WORKASPACE' ) );
#4039=ORIENTED_EDGE ( 'NONE', *, *, #3578, .F. ) ;
#4052=LINE ( 'NONE', #1183, #4711 ) ;
#4053=FACE_OUTER_BOUND ( 'NONE', #7266, .T. ) ;
#4055=ORIENTED_EDGE ( 'NONE', *, *, #5724, .F. ) ;
#4090=ORIENTED_EDGE ( 'NONE', *, *, #5913, .T. ) ;
#4099=ADVANCED_FACE ( 'NONE', ( #1416 ), #2639, .F. ) ;
#4104=CIRCLE ( 'NONE', #1826, 4.250000000000000000 ) ;
#4118=( NAMED_UNIT ( * ) PLANE_ANGLE_UNIT ( ) SI_UNIT ( $, .RADIAN. ) );
#4127=CYLINDRICAL_SURFACE ( 'NONE', #4616, 4.250000000000000000 ) ;
#4130=VECTOR ( 'NONE', #2751, 1000.000000000000000 ) ;
#4146=ORIENTED_EDGE ( 'NONE', *, *, #6333, .T. ) ;
#4162=FACE_OUTER_BOUND ( 'NONE', #6506, .T. ) ;
#4174=EDGE_CURVE ( 'NONE', #2423, #5618, #30, .T. ) ;
#4183=PRESENTATION_STYLE_ASSIGNMENT (( #823 ) ) ;
#4186=VECTOR ( 'NONE', #2219, 1000.000000000000114 ) ;
#4203=VERTEX_POINT ( 'NONE', #481 ) ;
#4208=ORIENTED_EDGE ( 'NONE', *, *, #2527, .F. ) ;
#4216=ORIENTED_EDGE ( 'NONE', *, *, #4356, .F. ) ;
#4249=ORIENTED_EDGE ( 'NONE', *, *, #418, .F. ) ;
#4258=PLANE ( 'NONE',  #4514 ) ;
#4266=EDGE_LOOP ( 'NONE', ( #4802, #2500, #1685 ) ) ;
#4273=LINE ( 'NONE', #5590, #1363 ) ;
#4275=DIRECTION ( 'NONE',  ( 0.000000000000000000, 1.224646799147353207E-16, 1.000000000000000000 ) ) ;
#4311=DIRECTION ( 'NONE',  ( -1.000000000000000000, -0.000000000000000000, -0.000000000000000000 ) ) ;
#4312=LINE ( 'NONE', #1355, #1007 ) ;
#4318=VERTEX_POINT ( 'NONE', #3447 ) ;
#4321=PLANE ( 'NONE',  #3988 ) ;
#4342=AXIS2_PLACEMENT_3D ( 'NONE', #318, #7126, #4275 ) ;
#4347=DIRECTION ( 'NONE',  ( 0.000000000000000000, 0.8660254037844380415, -0.5000000000000012212 ) ) ;
#4353=DIRECTION ( 'NONE',  ( 1.000000000000000000, 0.000000000000000000, 0.000000000000000000 ) ) ;
#4356=EDGE_CURVE ( 'NONE', #2028, #6041, #589, .T. ) ;
#4361=FACE_OUTER_BOUND ( 'NONE', #5097, .T. ) ;
#4378=EDGE_LOOP ( 'NONE', ( #3581, #5027, #4620, #404 ) ) ;
#4385=EDGE_LOOP ( 'NONE', ( #4090, #5146, #4682, #1866, #6316 ) ) ;
#4396=EDGE_CURVE ( 'NONE', #6971, #5618, #1182, .T. ) ;
#4397=LINE ( 'NONE', #2699, #3387 ) ;
#4401=DIRECTION ( 'NONE',  ( -1.000000000000000000, -0.000000000000000000, -0.000000000000000000 ) ) ;
#4403=CARTESIAN_POINT ( 'NONE',  ( 2.500000000000000000, 0.000000000000000000, 0.000000000000000000 ) ) ;
#4428=DIRECTION ( 'NONE',  ( 0.000000000000000000, 0.000000000000000000, 1.000000000000000000 ) ) ;
#4429=DIRECTION ( 'NONE',  ( 0.000000000000000000, 0.000000000000000000, 1.000000000000000000 ) ) ;
#4435=DIRECTION ( 'NONE',  ( 0.000000000000000000, 0.000000000000000000, 1.000000000000000000 ) ) ;
#4436=DIRECTION ( 'NONE',  ( 0.000000000000000000, 0.000000000000000000, 1.000000000000000000 ) ) ;
#4437=DIRECTION ( 'NONE',  ( -1.000000000000000000, -0.000000000000000000, -0.000000000000000000 ) ) ;
#4452=FACE_OUTER_BOUND ( 'NONE', #3075, .T. ) ;
#4471=DIRECTION ( 'NONE',  ( -1.000000000000000000, -0.000000000000000000, -0.000000000000000000 ) ) ;
#4482=ORIENTED_EDGE ( 'NONE', *, *, #6042, .F. ) ;
#4486=CIRCLE ( 'NONE', #6514, 2.500000000000001332 ) ;
#4494=DIRECTION ( 'NONE',  ( -1.000000000000000000, -0.000000000000000000, -0.000000000000000000 ) ) ;
#4507=DIRECTION ( 'NONE',  ( 1.000000000000000000, 0.000000000000000000, 0.000000000000000000 ) ) ;
#4514=AXIS2_PLACEMENT_3D ( 'NONE', #7220, #1412, #3185 ) ;
#4521=DIRECTION ( 'NONE',  ( 0.000000000000000000, -0.8660254037844390407, -0.4999999999999994449 ) ) ;
#4532=DIRECTION ( 'NONE',  ( -1.000000000000000000, -0.000000000000000000, -0.000000000000000000 ) ) ;
#4553=ORIENTED_EDGE ( 'NONE', *, *, #3120, .T. ) ;
#4560=VECTOR ( 'NONE', #3653, 1000.000000000000000 ) ;
#4564=DIRECTION ( 'NONE',  ( 0.000000000000000000, 0.000000000000000000, -1.000000000000000000 ) ) ;
#4583=DIRECTION ( 'NONE',  ( 0.000000000000000000, -0.4999999999999992784, 0.8660254037844389297 ) ) ;
#4592=CIRCLE ( 'NONE', #2301, 4.000000000000000000 ) ;
#4593=ORIENTED_EDGE ( 'NONE', *, *, #4803, .T. ) ;
#4604=DIRECTION ( 'NONE',  ( 0.000000000000000000, -1.000000000000000000, 1.287488025362403787E-15 ) ) ;
#4606=ORIENTED_EDGE ( 'NONE', *, *, #418, .T. ) ;
#4616=AXIS2_PLACEMENT_3D ( 'NONE', #655, #6974, #2913 ) ;
#4620=ORIENTED_EDGE ( 'NONE', *, *, #5376, .T. ) ;
#4629=ADVANCED_FACE ( 'NONE', ( #3913 ), #6843, .T. ) ;
#4646=DIRECTION ( 'NONE',  ( -1.000000000000000000, -0.000000000000000000, -0.000000000000000000 ) ) ;
#4664=ORIENTED_EDGE ( 'NONE', *, *, #2459, .F. ) ;
#4670=LINE ( 'NONE', #7001, #4560 ) ;
#4675=DIRECTION ( 'NONE',  ( -1.000000000000000000, -0.000000000000000000, -0.000000000000000000 ) ) ;
#4682=ORIENTED_EDGE ( 'NONE', *, *, #70, .F. ) ;
#4685=PLANE ( 'NONE',  #6412 ) ;
#4698=( GEOMETRIC_REPRESENTATION_CONTEXT ( 3 ) GLOBAL_UNCERTAINTY_ASSIGNED_CONTEXT ( ( #2171 ) ) GLOBAL_UNIT_ASSIGNED_CONTEXT ( ( #3079, #4118, #265 ) ) REPRESENTATION_CONTEXT ( 'NONE', 'WORKASPACE' ) );
#4711=VECTOR ( 'NONE', #2817, 1000.000000000000000 ) ;
#4719=AXIS2_PLACEMENT_3D ( 'NONE', #2839, #1726, #1620 ) ;
#4721=EDGE_CURVE ( 'NONE', #7308, #2488, #1210, .T. ) ;
#4722=CARTESIAN_POINT ( 'NONE',  ( 2.500000000000000000, 2.357898499370433054, -1.951563910473907981E-15 ) ) ;
#4723=ORIENTED_EDGE ( 'NONE', *, *, #3551, .F. ) ;
#4731=DIRECTION ( 'NONE',  ( 1.000000000000000000, 0.000000000000000000, 0.000000000000000000 ) ) ;
#4738=CARTESIAN_POINT ( 'NONE',  ( 2.500000000000000000, 0.000000000000000000, 0.000000000000000000 ) ) ;
#4745=ORIENTED_EDGE ( 'NONE', *, *, #2507, .T. ) ;
#4752=DIRECTION ( 'NONE',  ( 1.000000000000000000, 0.000000000000000000, 0.000000000000000000 ) ) ;
#4753=CARTESIAN_POINT ( 'NONE',  ( -31.74999999999995737, 0.000000000000000000, 0.000000000000000000 ) ) ;
#4769=CARTESIAN_POINT ( 'NONE',  ( 0.2500000000000002220, 5.204748896376250699E-16, -4.250000000000000000 ) ) ;
#4770=ORIENTED_EDGE ( 'NONE', *, *, #4795, .F. ) ;
#4774=ORIENTED_EDGE ( 'NONE', *, *, #6333, .F. ) ;
#4795=EDGE_CURVE ( 'NONE', #2028, #2488, #2030, .T. ) ;
#4802=ORIENTED_EDGE ( 'NONE', *, *, #3390, .F. ) ;
#4803=EDGE_CURVE ( 'NONE', #2803, #2072, #654, .T. ) ;
#4813=CARTESIAN_POINT ( 'NONE',  ( 0.2500000000000002220, 0.000000000000000000, 0.000000000000000000 ) ) ;
#4818=TOROIDAL_SURFACE ( 'NONE', #4945, 4.000000000000000000, 0.2500000000000000000 ) ;
#4867=CARTESIAN_POINT ( 'NONE',  ( 2.500000000000000000, 2.357898499370433054, -1.951563910473907981E-15 ) ) ;
#4884=EDGE_LOOP ( 'NONE', ( #5928, #4039, #4606, #1102, #3545 ) ) ;
#4886=ORIENTED_EDGE ( 'NONE', *, *, #6042, .T. ) ;
#4893=DIRECTION ( 'NONE',  ( 0.000000000000000000, 0.4999999999999993339, -0.8660254037844390407 ) ) ;
#4901=ADVANCED_FACE ( 'NONE', ( #2009 ), #3239, .F. ) ;
#4918=FACE_OUTER_BOUND ( 'NONE', #127, .T. ) ;
#4929=VECTOR ( 'NONE', #2733, 1000.000000000000000 ) ;
#4938=CARTESIAN_POINT ( 'NONE',  ( 2.500000000000000000, 2.357898499370433054, -1.951563910473907981E-15 ) ) ;
#4945=AXIS2_PLACEMENT_3D ( 'NONE', #1464, #2103, #1428 ) ;
#4958=LINE ( 'NONE', #1981, #2410 ) ;
#4962=COLOUR_RGB ( '',1.000000000000000000, 0.9490196078431372140, 0.9098039215686274384 ) ;
#4968=DIRECTION ( 'NONE',  ( 1.000000000000000000, 0.000000000000000000, 0.000000000000000000 ) ) ;
#4973=ADVANCED_FACE ( 'NONE', ( #3782 ), #5863, .F. ) ;
#4977=AXIS2_PLACEMENT_3D ( 'NONE', #3950, #480, #2814 ) ;
#4992=DIRECTION ( 'NONE',  ( -0.000000000000000000, 0.000000000000000000, 1.000000000000000000 ) ) ;
#5000=EDGE_CURVE ( 'NONE', #468, #6247, #1313, .T. ) ;
#5001=DIRECTION ( 'NONE',  ( 0.000000000000000000, -0.5000000000000011102, -0.8660254037844379305 ) ) ;
#5002=LINE ( 'NONE', #6004, #6503 ) ;
#5026=EDGE_CURVE ( 'NONE', #3704, #5368, #3162, .T. ) ;
#5027=ORIENTED_EDGE ( 'NONE', *, *, #5520, .T. ) ;
#5032=LINE ( 'NONE', #435, #2644 ) ;
#5042=( NAMED_UNIT ( * ) SI_UNIT ( $, .STERADIAN. ) SOLID_ANGLE_UNIT ( ) );
#5052=ADVANCED_FACE ( 'NONE', ( #982 ), #3570, .T. ) ;
#5057=CARTESIAN_POINT ( 'NONE',  ( 2.500000000000000000, -2.629050547790028551E-15, -2.041999999999999815 ) ) ;
#5058=CIRCLE ( 'NONE', #2173, 4.250000000000000000 ) ;
#5059=CARTESIAN_POINT ( 'NONE',  ( 2.500000000000000000, 1.178949249685213863, -2.042000000000001148 ) ) ;
#5097=EDGE_LOOP ( 'NONE', ( #1451, #4146, #6849, #1185 ) ) ;
#5139=CARTESIAN_POINT ( 'NONE',  ( 0.2500000000000002220, 0.000000000000000000, 0.000000000000000000 ) ) ;
#5142=LINE ( 'NONE', #1688, #987 ) ;
#5146=ORIENTED_EDGE ( 'NONE', *, *, #1875, .F. ) ;
#5158=ORIENTED_EDGE ( 'NONE', *, *, #5865, .F. ) ;
#5160=LINE ( 'NONE', #5059, #3514 ) ;
#5178=DIRECTION ( 'NONE',  ( -1.000000000000000000, -0.000000000000000000, -0.000000000000000000 ) ) ;
#5197=VERTEX_POINT ( 'NONE', #5735 ) ;
#5198=VECTOR ( 'NONE', #3147, 1000.000000000000000 ) ;
#5203=DIRECTION ( 'NONE',  ( 0.000000000000000000, 0.000000000000000000, 1.000000000000000000 ) ) ;
#5218=LINE ( 'NONE', #66, #1012 ) ;
#5233=LINE ( 'NONE', #116, #2411 ) ;
#5265=DIRECTION ( 'NONE',  ( 1.000000000000000000, 0.000000000000000000, 0.000000000000000000 ) ) ;
#5275=CARTESIAN_POINT ( 'NONE',  ( 2.500000000000000000, 2.357898499370433054, -1.951563910473907981E-15 ) ) ;
#5277=ADVANCED_FACE ( 'NONE', ( #6442 ), #7006, .T. ) ;
#5296=VECTOR ( 'NONE', #2944, 1000.000000000000114 ) ;
#5305=EDGE_CURVE ( 'NONE', #5197, #1419, #3456, .T. ) ;
#5312=DIRECTION ( 'NONE',  ( -1.000000000000000000, -0.000000000000000000, -0.000000000000000000 ) ) ;
#5328=DIRECTION ( 'NONE',  ( 0.000000000000000000, -1.000000000000000000, 1.287488025362403787E-15 ) ) ;
#5332=ORIENTED_EDGE ( 'NONE', *, *, #3748, .T. ) ;
#5335=ADVANCED_FACE ( 'NONE', ( #6903 ), #1757, .T. ) ;
#5340=FACE_OUTER_BOUND ( 'NONE', #6835, .T. ) ;
#5345=CARTESIAN_POINT ( 'NONE',  ( 5.200000000000002842, 0.000000000000000000, 0.000000000000000000 ) ) ;
#5368=VERTEX_POINT ( 'NONE', #933 ) ;
#5376=EDGE_CURVE ( 'NONE', #5585, #586, #1447, .T. ) ;
#5416=DIRECTION ( 'NONE',  ( 0.000000000000000000, 0.000000000000000000, -1.000000000000000000 ) ) ;
#5431=DIRECTION ( 'NONE',  ( 0.000000000000000000, 0.000000000000000000, 1.000000000000000000 ) ) ;
#5440=AXIS2_PLACEMENT_3D ( 'NONE', #1104, #4471, #4435 ) ;
#5443=ORIENTED_EDGE ( 'NONE', *, *, #70, .T. ) ;
#5462=CARTESIAN_POINT ( 'NONE',  ( 2.500000000000000000, -2.357898499370432610, 3.252606517456513302E-15 ) ) ;
#5470=ORIENTED_EDGE ( 'NONE', *, *, #1571, .F. ) ;
#5476=EDGE_CURVE ( 'NONE', #2468, #1612, #3687, .T. ) ;
#5487=FACE_OUTER_BOUND ( 'NONE', #2919, .T. ) ;
#5488=ORIENTED_EDGE ( 'NONE', *, *, #5376, .F. ) ;
#5489=CARTESIAN_POINT ( 'NONE',  ( -31.74999999999995737, 0.000000000000000000, 4.250000000000000000 ) ) ;
#5490=FACE_OUTER_BOUND ( 'NONE', #518, .T. ) ;
#5497=AXIS2_PLACEMENT_3D ( 'NONE', #3818, #350, #313 ) ;
#5503=DIRECTION ( 'NONE',  ( 0.000000000000000000, -1.000000000000000000, 0.000000000000000000 ) ) ;
#5504=DIRECTION ( 'NONE',  ( -1.000000000000000000, -0.000000000000000000, -0.000000000000000000 ) ) ;
#5519=EDGE_LOOP ( 'NONE', ( #2366, #1615 ) ) ;
#5520=EDGE_CURVE ( 'NONE', #1382, #5585, #5058, .T. ) ;
#5528=ADVANCED_FACE ( 'NONE', ( #4452 ), #7333, .F. ) ;
#5564=DIRECTION ( 'NONE',  ( 0.000000000000000000, -1.000000000000000000, 1.287488025362403787E-15 ) ) ;
#5585=VERTEX_POINT ( 'NONE', #2720 ) ;
#5588=FACE_OUTER_BOUND ( 'NONE', #4266, .T. ) ;
#5590=CARTESIAN_POINT ( 'NONE',  ( 0.000000000000000000, -1.178949249685213863, 2.042000000000002924 ) ) ;
#5593=EDGE_CURVE ( 'NONE', #6342, #7102, #269, .T. ) ;
#5597=CARTESIAN_POINT ( 'NONE',  ( 0.000000000000000000, 0.000000000000000000, 0.000000000000000000 ) ) ;
#5599=( NAMED_UNIT ( * ) PLANE_ANGLE_UNIT ( ) SI_UNIT ( $, .RADIAN. ) );
#5601=CARTESIAN_POINT ( 'NONE',  ( 2.500000000000000000, 0.000000000000000000, 0.000000000000000000 ) ) ;
#5618=VERTEX_POINT ( 'NONE', #5057 ) ;
#5626=DIRECTION ( 'NONE',  ( 0.000000000000000000, 0.000000000000000000, -1.000000000000000000 ) ) ;
#5634=AXIS2_PLACEMENT_3D ( 'NONE', #1913, #3070, #4436 ) ;
#5635=EDGE_CURVE ( 'NONE', #977, #2423, #6367, .T. ) ;
#5638=EDGE_LOOP ( 'NONE', ( #5158, #1718, #5795, #3736, #773 ) ) ;
#5668=ORIENTED_EDGE ( 'NONE', *, *, #5000, .T. ) ;
#5671=CARTESIAN_POINT ( 'NONE',  ( 5.000000000000000888, 4.250000000000000000, 0.000000000000000000 ) ) ;
#5683=EDGE_CURVE ( 'NONE', #2446, #586, #6802, .T. ) ;
#5701=MANIFOLD_SOLID_BREP ( 'Hex', #1931 ) ;
#5709=EDGE_LOOP ( 'NONE', ( #4593, #3651, #938, #3435, #5964, #1093 ) ) ;
#5711=VECTOR ( 'NONE', #290, 1000.000000000000000 ) ;
#5715=DIRECTION ( 'NONE',  ( 0.000000000000000000, -0.4999999999999993894, 0.8660254037844389297 ) ) ;
#5724=EDGE_CURVE ( 'NONE', #7102, #6342, #2387, .T. ) ;
#5735=CARTESIAN_POINT ( 'NONE',  ( 5.200000000000002842, 3.061616997868384127E-16, -2.500000000000000888 ) ) ;
#5746=CARTESIAN_POINT ( 'NONE',  ( 0.000000000000000000, 2.357898499370433054, -1.951563910473907981E-15 ) ) ;
#5779=FACE_OUTER_BOUND ( 'NONE', #4378, .T. ) ;
#5788=CIRCLE ( 'NONE', #2536, 2.041999999999999815 ) ;
#5795=ORIENTED_EDGE ( 'NONE', *, *, #3018, .T. ) ;
#5811=AXIS2_PLACEMENT_3D ( 'NONE', #5597, #4401, #3914 ) ;
#5812=FILL_AREA_STYLE ('',( #3257 ) ) ;
#5815=CARTESIAN_POINT ( 'NONE',  ( 0.000000000000000000, 2.357898499370433054, -1.951563910473907981E-15 ) ) ;
#5821=ADVANCED_FACE ( 'NONE', ( #326 ), #5994, .F. ) ;
#5829=DIRECTION ( 'NONE',  ( 1.000000000000000000, 0.000000000000000000, 0.000000000000000000 ) ) ;
#5839=EDGE_LOOP ( 'NONE', ( #6166, #1634, #1194, #3424 ) ) ;
#5847=EDGE_CURVE ( 'NONE', #6041, #2468, #4052, .T. ) ;
#5851=LINE ( 'NONE', #1146, #1850 ) ;
#5853=DIRECTION ( 'NONE',  ( 0.000000000000000000, -1.000000000000000000, 1.471414886128461471E-15 ) ) ;
#5860=ORIENTED_EDGE ( 'NONE', *, *, #7172, .T. ) ;
#5863=CONICAL_SURFACE ( 'NONE', #2373, 2.041999999999999815, 1.047197551196591858 ) ;
#5865=EDGE_CURVE ( 'NONE', #6971, #2488, #5218, .T. ) ;
#5876=DIRECTION ( 'NONE',  ( -1.000000000000000000, -0.000000000000000000, -0.000000000000000000 ) ) ;
#5891=CARTESIAN_POINT ( 'NONE',  ( 2.500000000000000000, 2.357898499370433054, -1.951563910473907981E-15 ) ) ;
#5913=EDGE_CURVE ( 'NONE', #2803, #4203, #29, .T. ) ;
#5917=STYLED_ITEM ( 'NONE', ( #4183 ), #7090 ) ;
#5928=ORIENTED_EDGE ( 'NONE', *, *, #6072, .F. ) ;
#5958=SURFACE_STYLE_FILL_AREA ( #5812 ) ;
#5964=ORIENTED_EDGE ( 'NONE', *, *, #500, .F. ) ;
#5974=EDGE_LOOP ( 'NONE', ( #1090, #280 ) ) ;
#5994=CONICAL_SURFACE ( 'NONE', #3580, 2.041999999999999815, 1.047197551196591858 ) ;
#6000=DIRECTION ( 'NONE',  ( 0.000000000000000000, 0.000000000000000000, 1.000000000000000000 ) ) ;
#6004=CARTESIAN_POINT ( 'NONE',  ( 2.500000000000000000, -1.178949249685218303, -2.041999999999998039 ) ) ;
#6010=ADVANCED_FACE ( 'NONE', ( #4162 ), #3666, .F. ) ;
#6012=ORIENTED_EDGE ( 'NONE', *, *, #2497, .T. ) ;
#6013=AXIS2_PLACEMENT_3D ( 'NONE', #7033, #4494, #6787 ) ;
#6016=CARTESIAN_POINT ( 'NONE',  ( -31.74999999999995737, 3.061616997868384127E-16, -2.500000000000000888 ) ) ;
#6017=CIRCLE ( 'NONE', #1930, 2.041999999999999815 ) ;
#6041=VERTEX_POINT ( 'NONE', #6382 ) ;
#6042=EDGE_CURVE ( 'NONE', #1419, #5197, #2305, .T. ) ;
#6054=AXIS2_PLACEMENT_3D ( 'NONE', #6332, #5265, #115 ) ;
#6058=CARTESIAN_POINT ( 'NONE',  ( -31.74999999999995737, 0.000000000000000000, 2.500000000000000888 ) ) ;
#6072=EDGE_CURVE ( 'NONE', #3535, #2468, #7051, .T. ) ;
#6078=DIRECTION ( 'NONE',  ( -1.000000000000000000, 0.000000000000000000, -0.000000000000000000 ) ) ;
#6079=ORIENTED_EDGE ( 'NONE', *, *, #500, .T. ) ;
#6097=CARTESIAN_POINT ( 'NONE',  ( 2.500000000000000000, -1.178949249685213863, 2.042000000000002924 ) ) ;
#6108=VERTEX_POINT ( 'NONE', #1031 ) ;
#6118=DIRECTION ( 'NONE',  ( -1.000000000000000000, -0.000000000000000000, -0.000000000000000000 ) ) ;
#6127=PLANE ( 'NONE',  #2558 ) ;
#6144=CARTESIAN_POINT ( 'NONE',  ( 5.000000000000004441, 0.000000000000000000, 0.000000000000000000 ) ) ;
#6155=AXIS2_PLACEMENT_3D ( 'NONE', #1399, #6535, #7204 ) ;
#6166=ORIENTED_EDGE ( 'NONE', *, *, #7172, .F. ) ;
#6180=CIRCLE ( 'NONE', #5440, 2.041999999999999815 ) ;
#6181=CARTESIAN_POINT ( 'NONE',  ( 2.500000000000000000, -1.178949249685213863, 2.042000000000002924 ) ) ;
#6195=ORIENTED_EDGE ( 'NONE', *, *, #5635, .T. ) ;
#6211=ORIENTED_EDGE ( 'NONE', *, *, #1318, .F. ) ;
#6220=EDGE_CURVE ( 'NONE', #3083, #598, #2314, .T. ) ;
#6241=EDGE_CURVE ( 'NONE', #3535, #2072, #4273, .T. ) ;
#6247=VERTEX_POINT ( 'NONE', #6566 ) ;
#6249=AXIS2_PLACEMENT_3D ( 'NONE', #3230, #7268, #6707 ) ;
#6251=ORIENTED_EDGE ( 'NONE', *, *, #768, .T. ) ;
#6253=AXIS2_PLACEMENT_3D ( 'NONE', #316, #5503, #6644 ) ;
#6255=VECTOR ( 'NONE', #4893, 1000.000000000000000 ) ;
#6278=CARTESIAN_POINT ( 'NONE',  ( 0.000000000000000000, -1.178949249685218303, -2.041999999999998039 ) ) ;
#6300=CIRCLE ( 'NONE', #4977, 2.055000000000000160 ) ;
#6316=ORIENTED_EDGE ( 'NONE', *, *, #2779, .T. ) ;
#6328=AXIS2_PLACEMENT_3D ( 'NONE', #6706, #571, #4564 ) ;
#6332=CARTESIAN_POINT ( 'NONE',  ( 2.500000000000000000, 2.357898499370433054, -1.951563910473907981E-15 ) ) ;
#6333=EDGE_CURVE ( 'NONE', #2446, #3965, #185, .T. ) ;
#6342=VERTEX_POINT ( 'NONE', #1066 ) ;
#6356=VECTOR ( 'NONE', #1665, 1000.000000000000114 ) ;
#6362=PLANE ( 'NONE',  #6054 ) ;
#6367=CIRCLE ( 'NONE', #6013, 2.041999999999999815 ) ;
#6382=CARTESIAN_POINT ( 'NONE',  ( 2.500000000000000000, -2.357898499370432610, 3.252606517456513302E-15 ) ) ;
#6387=ORIENTED_EDGE ( 'NONE', *, *, #4803, .F. ) ;
#6412=AXIS2_PLACEMENT_3D ( 'NONE', #2976, #691, #4583 ) ;
#6442=FACE_OUTER_BOUND ( 'NONE', #991, .T. ) ;
#6445=CARTESIAN_POINT ( 'NONE',  ( 25.00000000000000000, 0.000000000000000000, 0.000000000000000000 ) ) ;
#6453=CARTESIAN_POINT ( 'NONE',  ( 0.000000000000000000, -1.178949249685213863, 2.042000000000002924 ) ) ;
#6463=ADVANCED_FACE ( 'NONE', ( #1235 ), #3021, .T. ) ;
#6477=AXIS2_PLACEMENT_3D ( 'NONE', #1389, #7048, #1280 ) ;
#6491=CIRCLE ( 'NONE', #6253, 0.2500000000000002220 ) ;
#6497=VECTOR ( 'NONE', #5564, 1000.000000000000000 ) ;
#6503=VECTOR ( 'NONE', #4311, 1000.000000000000000 ) ;
#6506=EDGE_LOOP ( 'NONE', ( #1956, #2606, #6211, #3384, #6626 ) ) ;
#6514=AXIS2_PLACEMENT_3D ( 'NONE', #230, #4646, #160 ) ;
#6535=DIRECTION ( 'NONE',  ( -1.000000000000000000, -0.000000000000000000, -0.000000000000000000 ) ) ;
#6545=STYLED_ITEM('',(#7446),#5701);
#6549=ORIENTED_EDGE ( 'NONE', *, *, #2497, .F. ) ;
#6566=CARTESIAN_POINT ( 'NONE',  ( 24.55500000000002103, 3.061616997868384620E-16, -2.500000000000001332 ) ) ;
#6574=EDGE_CURVE ( 'NONE', #6247, #468, #4486, .T. ) ;
#6591=ADVANCED_FACE ( 'NONE', ( #745 ), #6934, .T. ) ;
#6598=CARTESIAN_POINT ( 'NONE',  ( 25.00000000000000000, 0.000000000000000000, 0.000000000000000000 ) ) ;
#6604=AXIS2_PLACEMENT_3D ( 'NONE', #2276, #1657, #3942 ) ;
#6626=ORIENTED_EDGE ( 'NONE', *, *, #3578, .T. ) ;
#6630=CARTESIAN_POINT ( 'NONE',  ( 0.000000000000000000, -2.357898499370432610, 3.252606517456513302E-15 ) ) ;
#6638=ORIENTED_EDGE ( 'NONE', *, *, #2459, .T. ) ;
#6644=DIRECTION ( 'NONE',  ( 0.000000000000000000, 0.000000000000000000, -1.000000000000000000 ) ) ;
#6654=CARTESIAN_POINT ( 'NONE',  ( 5.200000000000002842, 0.000000000000000000, 0.000000000000000000 ) ) ;
#6676=ORIENTED_EDGE ( 'NONE', *, *, #288, .T. ) ;
#6687=CARTESIAN_POINT ( 'NONE',  ( 2.500000000000000000, 3.004629197474318851E-15, 2.042000000000000259 ) ) ;
#6696=CARTESIAN_POINT ( 'NONE',  ( 5.200000000000002842, 0.000000000000000000, 2.500000000000000888 ) ) ;
#6706=CARTESIAN_POINT ( 'NONE',  ( 5.200000000000002842, 0.000000000000000000, 0.000000000000000000 ) ) ;
#6707=DIRECTION ( 'NONE',  ( 0.000000000000000000, 0.000000000000000000, -1.000000000000000000 ) ) ;
#6709=AXIS2_PLACEMENT_3D ( 'NONE', #3537, #4675, #5203 ) ;
#6787=DIRECTION ( 'NONE',  ( 0.000000000000000000, 0.000000000000000000, 1.000000000000000000 ) ) ;
#6798=DIRECTION ( 'NONE',  ( 0.000000000000000000, 0.000000000000000000, -1.000000000000000000 ) ) ;
#6802=CIRCLE ( 'NONE', #98, 4.250000000000000000 ) ;
#6811=DIRECTION ( 'NONE',  ( 0.000000000000000000, 0.4999999999999993894, -0.8660254037844389297 ) ) ;
#6822=DIRECTION ( 'NONE',  ( 0.000000000000000000, 0.000000000000000000, -1.000000000000000000 ) ) ;
#6829=ORIENTED_EDGE ( 'NONE', *, *, #1406, .F. ) ;
#6835=EDGE_LOOP ( 'NONE', ( #3, #7077, #3883 ) ) ;
#6837=EDGE_CURVE ( 'NONE', #6108, #5618, #5160, .T. ) ;
#6843=CONICAL_SURFACE ( 'NONE', #3579, 2.055000000000000160, 0.7853981633974721488 ) ;
#6849=ORIENTED_EDGE ( 'NONE', *, *, #1435, .F. ) ;
#6896=DIRECTION ( 'NONE',  ( 0.000000000000000000, 0.000000000000000000, 1.000000000000000000 ) ) ;
#6903=FACE_OUTER_BOUND ( 'NONE', #4884, .T. ) ;
#6928=ORIENTED_EDGE ( 'NONE', *, *, #4174, .F. ) ;
#6934=CYLINDRICAL_SURFACE ( 'NONE', #3758, 2.500000000000000888 ) ;
#6953=ORIENTED_EDGE ( 'NONE', *, *, #3120, .F. ) ;
#6969=CARTESIAN_POINT ( 'NONE',  ( 2.500000000000000000, 1.178949249685218525, 2.041999999999999371 ) ) ;
#6971=VERTEX_POINT ( 'NONE', #1810 ) ;
#6974=DIRECTION ( 'NONE',  ( -1.000000000000000000, -0.000000000000000000, -0.000000000000000000 ) ) ;
#6976=CARTESIAN_POINT ( 'NONE',  ( 2.500000000000000000, -1.178949249685213863, 2.042000000000002924 ) ) ;
#6979=CIRCLE ( 'NONE', #3733, 4.250000000000000000 ) ;
#6982=AXIS2_PLACEMENT_3D ( 'NONE', #32, #4521, #6811 ) ;
#6983=ORIENTED_EDGE ( 'NONE', *, *, #43, .F. ) ;
#7001=CARTESIAN_POINT ( 'NONE',  ( -31.74999999999995737, 5.204748896376250699E-16, -4.250000000000000000 ) ) ;
#7006=CYLINDRICAL_SURFACE ( 'NONE', #6709, 2.500000000000000888 ) ;
#7011=ORIENTED_EDGE ( 'NONE', *, *, #2190, .T. ) ;
#7017=CARTESIAN_POINT ( 'NONE',  ( 0.000000000000000000, 2.357898499370433054, -1.951563910473907981E-15 ) ) ;
#7033=CARTESIAN_POINT ( 'NONE',  ( 2.500000000000000000, 0.000000000000000000, 0.000000000000000000 ) ) ;
#7043=ADVANCED_FACE ( 'NONE', ( #5340 ), #6362, .F. ) ;
#7048=DIRECTION ( 'NONE',  ( -1.000000000000000000, -0.000000000000000000, -0.000000000000000000 ) ) ;
#7051=LINE ( 'NONE', #6453, #180 ) ;
#7057=CYLINDRICAL_SURFACE ( 'NONE', #6155, 4.250000000000000000 ) ;
#7076=DIRECTION ( 'NONE',  ( 0.000000000000000000, 0.000000000000000000, 1.000000000000000000 ) ) ;
#7077=ORIENTED_EDGE ( 'NONE', *, *, #1653, .F. ) ;
#7082=ORIENTED_EDGE ( 'NONE', *, *, #3800, .F. ) ;
#7090=ADVANCED_BREP_SHAPE_REPRESENTATION ( '', ( #5701, #1963 ), #4003 ) ;
#7102=VERTEX_POINT ( 'NONE', #255 ) ;
#7109=DIRECTION ( 'NONE',  ( 0.000000000000000000, 0.000000000000000000, 1.000000000000000000 ) ) ;
#7126=DIRECTION ( 'NONE',  ( 0.000000000000000000, 1.000000000000000000, -1.224646799147353207E-16 ) ) ;
#7169=CARTESIAN_POINT ( 'NONE',  ( 2.500000000000000000, 1.178949249685213863, -2.042000000000001148 ) ) ;
#7172=EDGE_CURVE ( 'NONE', #3083, #6247, #2512, .T. ) ;
#7190=FACE_OUTER_BOUND ( 'NONE', #2763, .T. ) ;
#7204=DIRECTION ( 'NONE',  ( 0.000000000000000000, 0.000000000000000000, 1.000000000000000000 ) ) ;
#7220=CARTESIAN_POINT ( 'NONE',  ( 2.500000000000000000, 1.178949249685213863, -2.042000000000001148 ) ) ;
#7255=DIRECTION ( 'NONE',  ( 0.000000000000000000, 0.000000000000000000, -1.000000000000000000 ) ) ;
#7266=EDGE_LOOP ( 'NONE', ( #6387, #364, #560, #48, #5332 ) ) ;
#7268=DIRECTION ( 'NONE',  ( 1.000000000000000000, 0.000000000000000000, 0.000000000000000000 ) ) ;
#7283=DIRECTION ( 'NONE',  ( -1.000000000000000000, -0.000000000000000000, -0.000000000000000000 ) ) ;
#7287=DIRECTION ( 'NONE',  ( 1.000000000000000000, 0.000000000000000000, 0.000000000000000000 ) ) ;
#7298=CARTESIAN_POINT ( 'NONE',  ( 2.500000000000000000, 1.178949249685213863, -2.042000000000001148 ) ) ;
#7308=VERTEX_POINT ( 'NONE', #6181 ) ;
#7333=TOROIDAL_SURFACE ( 'NONE', #6328, 2.700000000000001066, 0.2000000000000000111 ) ;
#7440=COLOUR_RGB('Black',0.12,0.14,0.17);
#7441=FILL_AREA_STYLE_COLOUR('',#7440);
#7442=FILL_AREA_STYLE('',(#7441));
#7443=SURFACE_STYLE_FILL_AREA(#7442);
#7444=SURFACE_SIDE_STYLE('',(#7443));
#7445=SURFACE_STYLE_USAGE(.BOTH.,#7444);
#7446=PRESENTATION_STYLE_ASSIGNMENT((#7445));
ENDSEC;
END-ISO-10303-21;
